ISO-10303-21;
HEADER;
FILE_DESCRIPTION (('STEP AP214'),
    '1' );
FILE_NAME ('angular contact ball bearing_68_iso_ISO 15 ABB - 1720 - 28,SI,NC,28_68.step',
    '2026-10-24T13:33:06',
    ( '' ),
    ( '' ),
    'SwSTEP 2.0',
    'SolidWorks 2026',
    '' );
FILE_SCHEMA (( 'AUTOMOTIVE_DESIGN' ));
ENDSEC;

DATA;
#9=EDGE_CURVE ( 'NONE', #9071, #5710, #2897, .T. ) ;
#10=DIRECTION ( 'NONE',  ( 0.000000000000000000, 0.000000000000000000, -1.000000000000000000 ) ) ;
#41=CARTESIAN_POINT ( 'NONE',  ( 2.000000000000001332, 13.29999999999999893, 0.000000000000000000 ) ) ;
#46=FACE_OUTER_BOUND ( 'NONE', #11584, .T. ) ;
#84=AXIS2_PLACEMENT_3D ( 'NONE', #4836, #3666, #8077 ) ;
#130=FILL_AREA_STYLE ('',( #3509 ) ) ;
#154=DIRECTION ( 'NONE',  ( 1.000000000000000000, 0.000000000000000000, 0.000000000000000000 ) ) ;
#185=DIRECTION ( 'NONE',  ( 1.000000000000000000, 0.000000000000000000, 0.000000000000000000 ) ) ;
#204=PRESENTATION_STYLE_ASSIGNMENT (( #4594 ) ) ;
#205=CYLINDRICAL_SURFACE ( 'NONE', #8810, 11.05000000000000071 ) ;
#208=SHAPE_REPRESENTATION ( 'angular contact ball bearing_68_iso_ISO 15 ABB - 1720 - 28,SI,NC,28_68', ( #14039 ), #11646 ) ;
#209=ORIENTED_EDGE ( 'NONE', *, *, #9578, .T. ) ;
#233=FACE_OUTER_BOUND ( 'NONE', #9286, .T. ) ;
#239=ORIENTED_EDGE ( 'NONE', *, *, #12866, .T. ) ;
#240=DIRECTION ( 'NONE',  ( 0.000000000000000000, 1.000000000000000000, -1.224646799147353207E-16 ) ) ;
#277=LINE ( 'NONE', #1310, #12003 ) ;
#282=ORIENTED_EDGE ( 'NONE', *, *, #2329, .T. ) ;
#284=ORIENTED_EDGE ( 'NONE', *, *, #11720, .T. ) ;
#292=DIRECTION ( 'NONE',  ( 0.000000000000000000, 0.000000000000000000, -1.000000000000000000 ) ) ;
#300=FACE_OUTER_BOUND ( 'NONE', #11789, .T. ) ;
#310=ORIENTED_EDGE ( 'NONE', *, *, #2589, .F. ) ;
#324=AXIS2_PLACEMENT_3D ( 'NONE', #905, #4134, #5226 ) ;
#361=CYLINDRICAL_SURFACE ( 'NONE', #6142, 12.77499999999999858 ) ;
#368=CYLINDRICAL_SURFACE ( 'NONE', #956, 10.72500000000000142 ) ;
#384=ORIENTED_EDGE ( 'NONE', *, *, #3098, .T. ) ;
#429=AXIS2_PLACEMENT_3D ( 'NONE', #11798, #3965, #8601 ) ;
#455=CIRCLE ( 'NONE', #13681, 0.2000000000000022593 ) ;
#465=FACE_BOUND ( 'NONE', #5251, .T. ) ;
#497=TOROIDAL_SURFACE ( 'NONE', #7925, 13.29999999999999893, 0.2000000000000027034 ) ;
#512=DIRECTION ( 'NONE',  ( -1.000000000000000000, -0.000000000000000000, -0.000000000000000000 ) ) ;
#566=VERTEX_POINT ( 'NONE', #14267 ) ;
#576=CIRCLE ( 'NONE', #10566, 12.44999999999999929 ) ;
#603=EDGE_CURVE ( 'NONE', #5710, #9112, #7307, .T. ) ;
#610=CIRCLE ( 'NONE', #14302, 12.77500000000000036 ) ;
#616=VECTOR ( 'NONE', #713, 1000.000000000000000 ) ;
#637=DIRECTION ( 'NONE',  ( -1.000000000000000000, -0.000000000000000000, -0.000000000000000000 ) ) ;
#640=FACE_OUTER_BOUND ( 'NONE', #1038, .T. ) ;
#656=CARTESIAN_POINT ( 'NONE',  ( -20.63749999999999574, 0.000000000000000000, 0.000000000000000000 ) ) ;
#700=CARTESIAN_POINT ( 'NONE',  ( -2.000000000000001776, 0.000000000000000000, 0.000000000000000000 ) ) ;
#708=UNCERTAINTY_MEASURE_WITH_UNIT (LENGTH_MEASURE( 1.000000000000000082E-05 ), #11198, 'distance_accuracy_value', 'NONE');
#713=DIRECTION ( 'NONE',  ( 1.000000000000000000, 0.000000000000000000, 0.000000000000000000 ) ) ;
#728=EDGE_CURVE ( 'NONE', #4230, #2998, #2381, .T. ) ;
#742=AXIS2_PLACEMENT_3D ( 'NONE', #12289, #7713, #2203 ) ;
#758=EDGE_CURVE ( 'NONE', #13517, #7253, #6624, .T. ) ;
#765=EDGE_CURVE ( 'NONE', #9549, #5968, #7772, .T. ) ;
#783=ORIENTED_EDGE ( 'NONE', *, *, #12944, .F. ) ;
#785=ADVANCED_FACE ( 'NONE', ( #6941 ), #9638, .T. ) ;
#811=CARTESIAN_POINT ( 'NONE',  ( 1.800000000000001155, 0.000000000000000000, 0.000000000000000000 ) ) ;
#843=DIRECTION ( 'NONE',  ( 1.000000000000000000, 0.000000000000000000, 0.000000000000000000 ) ) ;
#846=FACE_OUTER_BOUND ( 'NONE', #14097, .T. ) ;
#885=AXIS2_PLACEMENT_3D ( 'NONE', #13105, #14263, #2302 ) ;
#888=CARTESIAN_POINT ( 'NONE',  ( -20.63749999999999929, 1.313433692085536673E-15, 10.72500000000000142 ) ) ;
#905=CARTESIAN_POINT ( 'NONE',  ( -0.7826237921249277196, 0.000000000000000000, 0.000000000000000000 ) ) ;
#923=CIRCLE ( 'NONE', #1166, 13.29999999999999893 ) ;
#956=AXIS2_PLACEMENT_3D ( 'NONE', #8003, #1190, #5637 ) ;
#961=MECHANICAL_DESIGN_GEOMETRIC_PRESENTATION_REPRESENTATION('',(#5399),#6555);
#984=ORIENTED_EDGE ( 'NONE', *, *, #765, .F. ) ;
#987=ORIENTED_EDGE ( 'NONE', *, *, #3098, .F. ) ;
#1033=ORIENTED_EDGE ( 'NONE', *, *, #13741, .F. ) ;
#1038=EDGE_LOOP ( 'NONE', ( #284, #8064, #9090, #7106 ) ) ;
#1049=TOROIDAL_SURFACE ( 'NONE', #4558, 10.20000000000000107, 0.2000000000000031197 ) ;
#1089=EDGE_CURVE ( 'NONE', #12823, #2998, #6949, .T. ) ;
#1099=CARTESIAN_POINT ( 'NONE',  ( -2.000000000000001776, 1.641026710857453312E-15, 13.29999999999999893 ) ) ;
#1105=AXIS2_PLACEMENT_3D ( 'NONE', #1329, #11353, #13588 ) ;
#1148=EDGE_LOOP ( 'NONE', ( #13554, #3782, #7353, #9523 ) ) ;
#1165=SURFACE_STYLE_FILL_AREA ( #130 ) ;
#1166=AXIS2_PLACEMENT_3D ( 'NONE', #9397, #12514, #7069 ) ;
#1190=DIRECTION ( 'NONE',  ( 1.000000000000000000, 0.000000000000000000, 0.000000000000000000 ) ) ;
#1213=AXIS2_PLACEMENT_3D ( 'NONE', #3991, #6162, #7918 ) ;
#1229=DIRECTION ( 'NONE',  ( -1.000000000000000000, -0.000000000000000000, -0.000000000000000000 ) ) ;
#1232=PRODUCT_DEFINITION_SHAPE ( 'NONE', 'NONE',  #6314 ) ;
#1234=( LENGTH_UNIT ( ) NAMED_UNIT ( * ) SI_UNIT ( .MILLI., .METRE. ) );
#1263=DIRECTION ( 'NONE',  ( -1.000000000000000000, -0.000000000000000000, -0.000000000000000000 ) ) ;
#1275=VERTEX_POINT ( 'NONE', #12852 ) ;
#1303=CARTESIAN_POINT ( 'NONE',  ( -0.2277608394786177770, 0.000000000000000000, 0.000000000000000000 ) ) ;
#1310=CARTESIAN_POINT ( 'NONE',  ( -20.63749999999999574, 0.000000000000000000, -12.44999999999999929 ) ) ;
#1314=STYLED_ITEM('',(#14410),#8329);
#1327=CARTESIAN_POINT ( 'NONE',  ( -1.799999999999996048, 1.224646799147353059E-15, 9.999999999999998224 ) ) ;
#1329=CARTESIAN_POINT ( 'NONE',  ( 1.800000000000001155, 0.000000000000000000, -13.29999999999999893 ) ) ;
#1330=CARTESIAN_POINT ( 'NONE',  ( 1.999999999999994893, 0.000000000000000000, 0.000000000000000000 ) ) ;
#1351=ORIENTED_EDGE ( 'NONE', *, *, #11461, .T. ) ;
#1388=CARTESIAN_POINT ( 'NONE',  ( 2.000000000000001776, 0.000000000000000000, 0.000000000000000000 ) ) ;
#1420=DIRECTION ( 'NONE',  ( -0.000000000000000000, 0.000000000000000000, 1.000000000000000000 ) ) ;
#1433=DIRECTION ( 'NONE',  ( 1.000000000000000000, 0.000000000000000000, 0.000000000000000000 ) ) ;
#1467=DIRECTION ( 'NONE',  ( 0.000000000000000000, 0.000000000000000000, -1.000000000000000000 ) ) ;
#1468=CARTESIAN_POINT ( 'NONE',  ( 1.800000000000001155, 1.628780242865979758E-15, 13.29999999999999893 ) ) ;
#1506=AXIS2_PLACEMENT_3D ( 'NONE', #11230, #240, #8839 ) ;
#1519=DIRECTION ( 'NONE',  ( 0.000000000000000000, 0.000000000000000000, -1.000000000000000000 ) ) ;
#1615=AXIS2_PLACEMENT_3D ( 'NONE', #13114, #843, #12984 ) ;
#1623=CYLINDRICAL_SURFACE ( 'NONE', #13952, 11.05000000000000071 ) ;
#1633=VECTOR ( 'NONE', #12005, 1000.000000000000000 ) ;
#1679=ADVANCED_FACE ( 'NONE', ( #2667 ), #2934, .T. ) ;
#1737=EDGE_CURVE ( 'NONE', #7052, #14164, #9096, .T. ) ;
#1750=CARTESIAN_POINT ( 'NONE',  ( -20.63749999999999929, 1.353234713057825478E-15, 11.05000000000000071 ) ) ;
#1751=TOROIDAL_SURFACE ( 'NONE', #9875, 13.29999999999999893, 0.2000000000000027034 ) ;
#1755=CARTESIAN_POINT ( 'NONE',  ( -20.63749999999999574, 1.564486285910743648E-15, 12.77499999999999858 ) ) ;
#1784=TOROIDAL_SURFACE ( 'NONE', #13934, 13.29999999999999893, 0.2000000000000027034 ) ;
#1812=CARTESIAN_POINT ( 'NONE',  ( 0.000000000000000000, 0.000000000000000000, 0.000000000000000000 ) ) ;
#1813=ORIENTED_EDGE ( 'NONE', *, *, #10581, .F. ) ;
#1846=TOROIDAL_SURFACE ( 'NONE', #3702, 11.75000000000000000, 1.050000000000000266 ) ;
#1852=CIRCLE ( 'NONE', #9540, 13.50000000000000533 ) ;
#1858=ORIENTED_EDGE ( 'NONE', *, *, #728, .F. ) ;
#1907=CARTESIAN_POINT ( 'NONE',  ( -1.799999999999996048, 0.000000000000000000, 0.000000000000000000 ) ) ;
#1913=LINE ( 'NONE', #1755, #1633 ) ;
#1917=EDGE_CURVE ( 'NONE', #7052, #10809, #14121, .T. ) ;
#1922=AXIS2_PLACEMENT_3D ( 'NONE', #7315, #6093, #11752 ) ;
#1961=ADVANCED_FACE ( 'NONE', ( #4276 ), #8696, .F. ) ;
#2014=MECHANICAL_DESIGN_GEOMETRIC_PRESENTATION_REPRESENTATION('',(#1314),#4345);
#2048=DIRECTION ( 'NONE',  ( 1.000000000000000000, 0.000000000000000000, 0.000000000000000000 ) ) ;
#2068=ORIENTED_EDGE ( 'NONE', *, *, #3577, .F. ) ;
#2073=CARTESIAN_POINT ( 'NONE',  ( -1.999999999999998224, 1.353234713057825478E-15, 11.05000000000000071 ) ) ;
#2076=ORIENTED_EDGE ( 'NONE', *, *, #10879, .T. ) ;
#2110=CIRCLE ( 'NONE', #3967, 10.20000000000000107 ) ;
#2124=DIRECTION ( 'NONE',  ( 0.000000000000000000, 0.000000000000000000, -1.000000000000000000 ) ) ;
#2131=DIRECTION ( 'NONE',  ( 1.000000000000000000, 0.000000000000000000, 0.000000000000000000 ) ) ;
#2158=EDGE_LOOP ( 'NONE', ( #8217, #6367, #13265, #7040 ) ) ;
#2203=DIRECTION ( 'NONE',  ( 0.000000000000000000, 0.000000000000000000, -1.000000000000000000 ) ) ;
#2222=EDGE_LOOP ( 'NONE', ( #209, #9361, #13489, #1858 ) ) ;
#2247=LINE ( 'NONE', #3420, #3118 ) ;
#2260=EDGE_LOOP ( 'NONE', ( #10953, #2981, #1033, #4159 ) ) ;
#2263=EDGE_LOOP ( 'NONE', ( #310, #8285, #6161, #4078 ) ) ;
#2264=LINE ( 'NONE', #7836, #8506 ) ;
#2267=AXIS2_PLACEMENT_3D ( 'NONE', #9991, #1263, #4486 ) ;
#2302=DIRECTION ( 'NONE',  ( 0.000000000000000000, 0.000000000000000000, -1.000000000000000000 ) ) ;
#2319=DIRECTION ( 'NONE',  ( 1.000000000000000000, 0.000000000000000000, 0.000000000000000000 ) ) ;
#2329=EDGE_CURVE ( 'NONE', #3772, #12248, #11464, .T. ) ;
#2364=DIRECTION ( 'NONE',  ( 0.000000000000000000, 0.000000000000000000, -1.000000000000000000 ) ) ;
#2380=EDGE_CURVE ( 'NONE', #9549, #4302, #12862, .T. ) ;
#2381=LINE ( 'NONE', #12383, #7990 ) ;
#2384=CARTESIAN_POINT ( 'NONE',  ( 1.999999999999998668, 1.249139735130300365E-15, 10.20000000000000107 ) ) ;
#2390=CARTESIAN_POINT ( 'NONE',  ( 1.799999999999996048, 0.000000000000000000, 0.000000000000000000 ) ) ;
#2400=ADVANCED_FACE ( 'NONE', ( #12300 ), #361, .F. ) ;
#2409=CARTESIAN_POINT ( 'NONE',  ( -20.63749999999999929, 1.224646799147352862E-15, 9.999999999999996447 ) ) ;
#2417=VERTEX_POINT ( 'NONE', #11493 ) ;
#2426=CARTESIAN_POINT ( 'NONE',  ( -20.63749999999999574, 0.000000000000000000, 0.000000000000000000 ) ) ;
#2443=EDGE_CURVE ( 'NONE', #12248, #3772, #2661, .T. ) ;
#2445=DIRECTION ( 'NONE',  ( 1.000000000000000000, 0.000000000000000000, 0.000000000000000000 ) ) ;
#2493=TOROIDAL_SURFACE ( 'NONE', #2267, 11.75000000000000000, 1.050000000000000266 ) ;
#2527=PLANE ( 'NONE',  #10913 ) ;
#2588=LINE ( 'NONE', #10564, #4334 ) ;
#2589=EDGE_CURVE ( 'NONE', #10676, #2417, #9716, .T. ) ;
#2591=CARTESIAN_POINT ( 'NONE',  ( 1.799999999999996048, 0.000000000000000000, 0.000000000000000000 ) ) ;
#2661=CIRCLE ( 'NONE', #6836, 10.72499999999999964 ) ;
#2667=FACE_OUTER_BOUND ( 'NONE', #3289, .T. ) ;
#2711=DIRECTION ( 'NONE',  ( 1.000000000000000000, 0.000000000000000000, 0.000000000000000000 ) ) ;
#2744=FACE_BOUND ( 'NONE', #5201, .T. ) ;
#2747=DIRECTION ( 'NONE',  ( 0.000000000000000000, 0.000000000000000000, -1.000000000000000000 ) ) ;
#2757=CARTESIAN_POINT ( 'NONE',  ( 0.2277608394786177770, 0.000000000000000000, 0.000000000000000000 ) ) ;
#2766=VERTEX_POINT ( 'NONE', #6246 ) ;
#2799=AXIS2_PLACEMENT_3D ( 'NONE', #12668, #3686, #10575 ) ;
#2806=AXIS2_PLACEMENT_3D ( 'NONE', #7241, #3831, #12678 ) ;
#2820=CARTESIAN_POINT ( 'NONE',  ( 1.999999999999998224, 0.000000000000000000, 0.000000000000000000 ) ) ;
#2840=FACE_OUTER_BOUND ( 'NONE', #7947, .T. ) ;
#2855=AXIS2_PLACEMENT_3D ( 'NONE', #11790, #3957, #5129 ) ;
#2859=ORIENTED_EDGE ( 'NONE', *, *, #3725, .T. ) ;
#2871=DIRECTION ( 'NONE',  ( 0.000000000000000000, 0.000000000000000000, 1.000000000000000000 ) ) ;
#2873=EDGE_LOOP ( 'NONE', ( #3414, #9238, #9236, #1813 ) ) ;
#2877=DIRECTION ( 'NONE',  ( 1.000000000000000000, 0.000000000000000000, 0.000000000000000000 ) ) ;
#2897=CIRCLE ( 'NONE', #6822, 1.050000000000000488 ) ;
#2934=TOROIDAL_SURFACE ( 'NONE', #4779, 13.29999999999999893, 0.2000000000000027034 ) ;
#2938=ORIENTED_EDGE ( 'NONE', *, *, #12515, .F. ) ;
#2951=ORIENTED_EDGE ( 'NONE', *, *, #5553, .F. ) ;
#2960=EDGE_CURVE ( 'NONE', #2417, #12823, #2247, .T. ) ;
#2962=AXIS2_PLACEMENT_3D ( 'NONE', #13079, #9970, #11131 ) ;
#2973=CARTESIAN_POINT ( 'NONE',  ( 2.000000000000001776, 0.000000000000000000, -12.44999999999999929 ) ) ;
#2979=ORIENTED_EDGE ( 'NONE', *, *, #13741, .T. ) ;
#2981=ORIENTED_EDGE ( 'NONE', *, *, #6675, .T. ) ;
#2998=VERTEX_POINT ( 'NONE', #10015 ) ;
#3009=UNCERTAINTY_MEASURE_WITH_UNIT (LENGTH_MEASURE( 1.000000000000000082E-05 ), #1234, 'distance_accuracy_value', 'NONE');
#3018=ADVANCED_FACE ( 'NONE', ( #10894 ), #13126, .F. ) ;
#3039=PRODUCT_DEFINITION_CONTEXT ( 'detailed design', #5635, 'design' ) ;
#3074=ORIENTED_EDGE ( 'NONE', *, *, #1737, .F. ) ;
#3098=EDGE_CURVE ( 'NONE', #5006, #9112, #13444, .T. ) ;
#3118=VECTOR ( 'NONE', #2319, 1000.000000000000000 ) ;
#3134=DIRECTION ( 'NONE',  ( 0.000000000000000000, 0.000000000000000000, -1.000000000000000000 ) ) ;
#3165=CYLINDRICAL_SURFACE ( 'NONE', #742, 13.50000000000000355 ) ;
#3229=PRODUCT ( 'angular contact ball bearing_68_iso_ISO 15 ABB - 1720 - 28,SI,NC,28_68', 'angular contact ball bearing_68_iso_ISO 15 ABB - 1720 - 28,SI,NC,28_68', '', ( #8198 ) ) ;
#3287=ORIENTED_EDGE ( 'NONE', *, *, #6675, .F. ) ;
#3289=EDGE_LOOP ( 'NONE', ( #2068, #10541, #12566, #5550 ) ) ;
#3295=VERTEX_POINT ( 'NONE', #2973 ) ;
#3303=ADVANCED_FACE ( 'NONE', ( #465, #13761 ), #8243, .T. ) ;
#3308=AXIS2_PLACEMENT_3D ( 'NONE', #6678, #5586, #7887 ) ;
#3327=ORIENTED_EDGE ( 'NONE', *, *, #9058, .F. ) ;
#3343=AXIS2_PLACEMENT_3D ( 'NONE', #12052, #13062, #13273 ) ;
#3351=CARTESIAN_POINT ( 'NONE',  ( -1.999999999999998224, 0.000000000000000000, -11.05000000000000071 ) ) ;
#3392=AXIS2_PLACEMENT_3D ( 'NONE', #13263, #5708, #7742 ) ;
#3401=CIRCLE ( 'NONE', #12227, 11.05000000000000071 ) ;
#3414=ORIENTED_EDGE ( 'NONE', *, *, #6848, .T. ) ;
#3420=CARTESIAN_POINT ( 'NONE',  ( -20.63749999999999574, 1.653273178848927261E-15, 13.50000000000000355 ) ) ;
#3430=CIRCLE ( 'NONE', #2962, 13.29999999999999893 ) ;
#3436=DIRECTION ( 'NONE',  ( 1.000000000000000000, 0.000000000000000000, 0.000000000000000000 ) ) ;
#3456=EDGE_CURVE ( 'NONE', #2766, #7253, #4433, .T. ) ;
#3460=DIRECTION ( 'NONE',  ( 1.000000000000000000, 0.000000000000000000, 0.000000000000000000 ) ) ;
#3467=CARTESIAN_POINT ( 'NONE',  ( -1.799999999999996048, 0.000000000000000000, 0.000000000000000000 ) ) ;
#3480=DIRECTION ( 'NONE',  ( -0.000000000000000000, 1.000000000000000000, 1.224646799147353207E-16 ) ) ;
#3509=FILL_AREA_STYLE_COLOUR ( '', #4701 ) ;
#3541=CIRCLE ( 'NONE', #2855, 0.2000000000000022593 ) ;
#3542=ORIENTED_EDGE ( 'NONE', *, *, #11289, .F. ) ;
#3551=FACE_BOUND ( 'NONE', #11332, .T. ) ;
#3554=CARTESIAN_POINT ( 'NONE',  ( 0.000000000000000000, 1.438959988998140160E-15, -11.75000000000000000 ) ) ;
#3575=FACE_OUTER_BOUND ( 'NONE', #14225, .T. ) ;
#3577=EDGE_CURVE ( 'NONE', #12823, #5253, #455, .T. ) ;
#3604=DIRECTION ( 'NONE',  ( 0.000000000000000000, 0.000000000000000000, -1.000000000000000000 ) ) ;
#3613=DIRECTION ( 'NONE',  ( 1.000000000000000000, 0.000000000000000000, 0.000000000000000000 ) ) ;
#3618=DIRECTION ( 'NONE',  ( 0.000000000000000000, 0.000000000000000000, -1.000000000000000000 ) ) ;
#3631=AXIS2_PLACEMENT_3D ( 'NONE', #8951, #11347, #6987 ) ;
#3644=EDGE_CURVE ( 'NONE', #566, #9071, #1913, .T. ) ;
#3646=DIRECTION ( 'NONE',  ( 0.000000000000000000, 0.000000000000000000, -1.000000000000000000 ) ) ;
#3666=DIRECTION ( 'NONE',  ( 1.000000000000000000, 0.000000000000000000, 0.000000000000000000 ) ) ;
#3686=DIRECTION ( 'NONE',  ( 1.000000000000000000, 0.000000000000000000, 0.000000000000000000 ) ) ;
#3702=AXIS2_PLACEMENT_3D ( 'NONE', #10551, #512, #2871 ) ;
#3717=ORIENTED_EDGE ( 'NONE', *, *, #728, .T. ) ;
#3725=EDGE_CURVE ( 'NONE', #2417, #4230, #1852, .T. ) ;
#3765=DIRECTION ( 'NONE',  ( -0.000000000000000000, 1.000000000000000000, 1.224646799147353207E-16 ) ) ;
#3772=VERTEX_POINT ( 'NONE', #13785 ) ;
#3782=ORIENTED_EDGE ( 'NONE', *, *, #7821, .F. ) ;
#3784=DIRECTION ( 'NONE',  ( 0.000000000000000000, 0.000000000000000000, -1.000000000000000000 ) ) ;
#3802=DIRECTION ( 'NONE',  ( 0.000000000000000000, -1.000000000000000000, 0.000000000000000000 ) ) ;
#3824=ORIENTED_EDGE ( 'NONE', *, *, #758, .F. ) ;
#3826=ADVANCED_FACE ( 'NONE', ( #3575 ), #205, .T. ) ;
#3831=DIRECTION ( 'NONE',  ( -1.000000000000000000, 0.000000000000000000, -0.000000000000000000 ) ) ;
#3849=DIRECTION ( 'NONE',  ( 1.000000000000000000, 0.000000000000000000, 0.000000000000000000 ) ) ;
#3867=CARTESIAN_POINT ( 'NONE',  ( 1.999999999999994893, 1.313433692085536476E-15, 10.72499999999999964 ) ) ;
#3880=EDGE_LOOP ( 'NONE', ( #7690, #5200 ) ) ;
#3893=DIRECTION ( 'NONE',  ( 1.000000000000000000, 0.000000000000000000, 0.000000000000000000 ) ) ;
#3901=FACE_BOUND ( 'NONE', #4803, .T. ) ;
#3919=DIRECTION ( 'NONE',  ( -1.000000000000000000, -0.000000000000000000, -0.000000000000000000 ) ) ;
#3928=ORIENTED_EDGE ( 'NONE', *, *, #7805, .T. ) ;
#3946=DIRECTION ( 'NONE',  ( 1.000000000000000000, 0.000000000000000000, 0.000000000000000000 ) ) ;
#3957=DIRECTION ( 'NONE',  ( 0.000000000000000000, -1.000000000000000000, 0.000000000000000000 ) ) ;
#3965=DIRECTION ( 'NONE',  ( 1.000000000000000000, 0.000000000000000000, 0.000000000000000000 ) ) ;
#3967=AXIS2_PLACEMENT_3D ( 'NONE', #13098, #14117, #9632 ) ;
#3991=CARTESIAN_POINT ( 'NONE',  ( -1.800000000000001155, 0.000000000000000000, -13.29999999999999893 ) ) ;
#4063=DIRECTION ( 'NONE',  ( 0.000000000000000000, 0.000000000000000000, -1.000000000000000000 ) ) ;
#4078=ORIENTED_EDGE ( 'NONE', *, *, #3725, .F. ) ;
#4134=DIRECTION ( 'NONE',  ( 1.000000000000000000, 0.000000000000000000, 0.000000000000000000 ) ) ;
#4135=ORIENTED_EDGE ( 'NONE', *, *, #7821, .T. ) ;
#4140=EDGE_LOOP ( 'NONE', ( #7914, #7190, #12359, #12426 ) ) ;
#4159=ORIENTED_EDGE ( 'NONE', *, *, #12866, .F. ) ;
#4160=DIRECTION ( 'NONE',  ( 0.000000000000000000, 0.000000000000000000, -1.000000000000000000 ) ) ;
#4172=DIRECTION ( 'NONE',  ( 0.000000000000000000, 0.000000000000000000, -1.000000000000000000 ) ) ;
#4187=VERTEX_POINT ( 'NONE', #13620 ) ;
#4190=ORIENTED_EDGE ( 'NONE', *, *, #5427, .F. ) ;
#4215=CARTESIAN_POINT ( 'NONE',  ( 2.000000000000001776, 0.000000000000000000, 0.000000000000000000 ) ) ;
#4230=VERTEX_POINT ( 'NONE', #12396 ) ;
#4276=FACE_OUTER_BOUND ( 'NONE', #11088, .T. ) ;
#4283=DIRECTION ( 'NONE',  ( 1.000000000000000000, 0.000000000000000000, 0.000000000000000000 ) ) ;
#4302=VERTEX_POINT ( 'NONE', #10876 ) ;
#4318=FACE_OUTER_BOUND ( 'NONE', #6945, .T. ) ;
#4334=VECTOR ( 'NONE', #3893, 1000.000000000000000 ) ;
#4345=( GEOMETRIC_REPRESENTATION_CONTEXT ( 3 ) GLOBAL_UNCERTAINTY_ASSIGNED_CONTEXT ( ( #3009 ) ) GLOBAL_UNIT_ASSIGNED_CONTEXT ( ( #1234, #13559, #7768 ) ) REPRESENTATION_CONTEXT ( 'NONE', 'WORKASPACE' ) );
#4409=CIRCLE ( 'NONE', #429, 13.29999999999999893 ) ;
#4430=DIRECTION ( 'NONE',  ( 0.000000000000000000, -1.224646799147352468E-16, 1.000000000000000000 ) ) ;
#4432=DIRECTION ( 'NONE',  ( 1.000000000000000000, 0.000000000000000000, 0.000000000000000000 ) ) ;
#4433=CIRCLE ( 'NONE', #11148, 0.2000000000000022593 ) ;
#4461=CIRCLE ( 'NONE', #8135, 13.50000000000000533 ) ;
#4486=DIRECTION ( 'NONE',  ( 0.000000000000000000, 0.000000000000000000, 1.000000000000000000 ) ) ;
#4510=ADVANCED_FACE ( 'NONE', ( #8835 ), #5428, .F. ) ;
#4524=( NAMED_UNIT ( * ) PLANE_ANGLE_UNIT ( ) SI_UNIT ( $, .RADIAN. ) );
#4548=CIRCLE ( 'NONE', #11964, 10.20000000000000107 ) ;
#4558=AXIS2_PLACEMENT_3D ( 'NONE', #3467, #11091, #5640 ) ;
#4594=SURFACE_STYLE_USAGE ( .BOTH. , #11335 ) ;
#4596=DIRECTION ( 'NONE',  ( 1.000000000000000000, 0.000000000000000000, 0.000000000000000000 ) ) ;
#4599=ORIENTED_EDGE ( 'NONE', *, *, #9, .T. ) ;
#4600=ORIENTED_EDGE ( 'NONE', *, *, #1917, .F. ) ;
#4612=ADVANCED_FACE ( 'NONE', ( #300 ), #13644, .T. ) ;
#4701=COLOUR_RGB ( '',1.000000000000000000, 0.9490196078431372140, 0.9098039215686274384 ) ;
#4714=ORIENTED_EDGE ( 'NONE', *, *, #2329, .F. ) ;
#4757=DIRECTION ( 'NONE',  ( 1.000000000000000000, 0.000000000000000000, 0.000000000000000000 ) ) ;
#4779=AXIS2_PLACEMENT_3D ( 'NONE', #7239, #13902, #11666 ) ;
#4803=EDGE_LOOP ( 'NONE', ( #13174, #1351 ) ) ;
#4817=ORIENTED_EDGE ( 'NONE', *, *, #5553, .T. ) ;
#4836=CARTESIAN_POINT ( 'NONE',  ( 1.999999999999994893, 0.000000000000000000, 0.000000000000000000 ) ) ;
#4868=EDGE_CURVE ( 'NONE', #5253, #11990, #4409, .T. ) ;
#4931=DIRECTION ( 'NONE',  ( -1.000000000000000000, -0.000000000000000000, -0.000000000000000000 ) ) ;
#4935=EDGE_CURVE ( 'NONE', #7052, #12248, #10864, .T. ) ;
#4945=ORIENTED_EDGE ( 'NONE', *, *, #7469, .T. ) ;
#4946=CARTESIAN_POINT ( 'NONE',  ( 1.800000000000002931, 1.653273178848927261E-15, 13.50000000000000178 ) ) ;
#4963=VERTEX_POINT ( 'NONE', #2073 ) ;
#4980=DIRECTION ( 'NONE',  ( 0.000000000000000000, 0.000000000000000000, -1.000000000000000000 ) ) ;
#5006=VERTEX_POINT ( 'NONE', #8895 ) ;
#5032=CIRCLE ( 'NONE', #3631, 12.77500000000000036 ) ;
#5033=ORIENTED_EDGE ( 'NONE', *, *, #9762, .F. ) ;
#5077=DIRECTION ( 'NONE',  ( 1.000000000000000000, 0.000000000000000000, 0.000000000000000000 ) ) ;
#5090=DIRECTION ( 'NONE',  ( 0.000000000000000000, 0.000000000000000000, 1.000000000000000000 ) ) ;
#5095=EDGE_CURVE ( 'NONE', #2998, #11990, #11813, .T. ) ;
#5129=DIRECTION ( 'NONE',  ( 0.000000000000000000, 0.000000000000000000, -1.000000000000000000 ) ) ;
#5167=CARTESIAN_POINT ( 'NONE',  ( -20.63749999999999929, 0.000000000000000000, -11.05000000000000071 ) ) ;
#5195=FACE_OUTER_BOUND ( 'NONE', #13267, .T. ) ;
#5200=ORIENTED_EDGE ( 'NONE', *, *, #5492, .F. ) ;
#5201=EDGE_LOOP ( 'NONE', ( #6609, #3542 ) ) ;
#5225=ORIENTED_EDGE ( 'NONE', *, *, #12168, .F. ) ;
#5226=DIRECTION ( 'NONE',  ( 0.000000000000000000, 0.000000000000000000, -1.000000000000000000 ) ) ;
#5251=EDGE_LOOP ( 'NONE', ( #5575, #14173 ) ) ;
#5253=VERTEX_POINT ( 'NONE', #11216 ) ;
#5262=ADVANCED_FACE ( 'NONE', ( #12802 ), #1846, .T. ) ;
#5271=CARTESIAN_POINT ( 'NONE',  ( 2.000000000000001776, 0.000000000000000000, -13.29999999999999893 ) ) ;
#5285=CIRCLE ( 'NONE', #13365, 11.05000000000000071 ) ;
#5399=STYLED_ITEM ( 'NONE', ( #204 ), #7317 ) ;
#5427=EDGE_CURVE ( 'NONE', #4302, #7253, #12074, .T. ) ;
#5428=CYLINDRICAL_SURFACE ( 'NONE', #885, 12.77499999999999858 ) ;
#5450=ORIENTED_EDGE ( 'NONE', *, *, #13006, .F. ) ;
#5492=EDGE_CURVE ( 'NONE', #10676, #1275, #3430, .T. ) ;
#5498=AXIS2_PLACEMENT_3D ( 'NONE', #5891, #4596, #3646 ) ;
#5539=CARTESIAN_POINT ( 'NONE',  ( -1.800000000000001155, 1.628780242865979758E-15, 13.29999999999999893 ) ) ;
#5540=CARTESIAN_POINT ( 'NONE',  ( -1.800000000000002931, 0.000000000000000000, 0.000000000000000000 ) ) ;
#5550=ORIENTED_EDGE ( 'NONE', *, *, #4868, .F. ) ;
#5553=EDGE_CURVE ( 'NONE', #7253, #13517, #5731, .T. ) ;
#5575=ORIENTED_EDGE ( 'NONE', *, *, #12944, .T. ) ;
#5586=DIRECTION ( 'NONE',  ( 1.000000000000000000, 0.000000000000000000, 0.000000000000000000 ) ) ;
#5597=EDGE_LOOP ( 'NONE', ( #14126, #783, #10410, #2938 ) ) ;
#5607=EDGE_CURVE ( 'NONE', #12252, #3295, #277, .T. ) ;
#5615=VERTEX_POINT ( 'NONE', #10309 ) ;
#5635=APPLICATION_CONTEXT ( 'automotive_design' ) ;
#5637=DIRECTION ( 'NONE',  ( 0.000000000000000000, 0.000000000000000000, -1.000000000000000000 ) ) ;
#5639=ORIENTED_EDGE ( 'NONE', *, *, #9, .F. ) ;
#5640=DIRECTION ( 'NONE',  ( 0.000000000000000000, 0.000000000000000000, -1.000000000000000000 ) ) ;
#5672=( NAMED_UNIT ( * ) PLANE_ANGLE_UNIT ( ) SI_UNIT ( $, .RADIAN. ) );
#5708=DIRECTION ( 'NONE',  ( 1.000000000000000000, 0.000000000000000000, 0.000000000000000000 ) ) ;
#5709=AXIS2_PLACEMENT_3D ( 'NONE', #8068, #13254, #13318 ) ;
#5710=VERTEX_POINT ( 'NONE', #11768 ) ;
#5731=CIRCLE ( 'NONE', #5498, 9.999999999999994671 ) ;
#5753=ORIENTED_EDGE ( 'NONE', *, *, #3456, .F. ) ;
#5776=DIRECTION ( 'NONE',  ( 1.000000000000000000, 0.000000000000000000, 0.000000000000000000 ) ) ;
#5779=VECTOR ( 'NONE', #11144, 1000.000000000000000 ) ;
#5784=DIRECTION ( 'NONE',  ( 0.000000000000000000, 0.000000000000000000, -1.000000000000000000 ) ) ;
#5826=EDGE_CURVE ( 'NONE', #6215, #5006, #6250, .T. ) ;
#5833=DIRECTION ( 'NONE',  ( 0.000000000000000000, 0.000000000000000000, -1.000000000000000000 ) ) ;
#5891=CARTESIAN_POINT ( 'NONE',  ( 1.799999999999996048, 0.000000000000000000, 0.000000000000000000 ) ) ;
#5956=CARTESIAN_POINT ( 'NONE',  ( -1.800000000000001155, 0.000000000000000000, 0.000000000000000000 ) ) ;
#5968=VERTEX_POINT ( 'NONE', #12663 ) ;
#6037=ORIENTED_EDGE ( 'NONE', *, *, #7373, .T. ) ;
#6065=CIRCLE ( 'NONE', #10717, 12.44999999999999929 ) ;
#6067=AXIS2_PLACEMENT_3D ( 'NONE', #10351, #9348, #11587 ) ;
#6087=CARTESIAN_POINT ( 'NONE',  ( 0.2277608394786177770, 1.419059478511995659E-15, -10.72500000000000142 ) ) ;
#6093=DIRECTION ( 'NONE',  ( 1.000000000000000000, 0.000000000000000000, 0.000000000000000000 ) ) ;
#6142=AXIS2_PLACEMENT_3D ( 'NONE', #12438, #4757, #7996 ) ;
#6149=FACE_OUTER_BOUND ( 'NONE', #2263, .T. ) ;
#6161=ORIENTED_EDGE ( 'NONE', *, *, #10859, .T. ) ;
#6162=DIRECTION ( 'NONE',  ( 0.000000000000000000, -1.000000000000000000, 0.000000000000000000 ) ) ;
#6188=AXIS2_PLACEMENT_3D ( 'NONE', #12131, #1229, #11190 ) ;
#6203=CARTESIAN_POINT ( 'NONE',  ( -20.63749999999999929, 0.000000000000000000, 0.000000000000000000 ) ) ;
#6215=VERTEX_POINT ( 'NONE', #11111 ) ;
#6226=AXIS2_PLACEMENT_3D ( 'NONE', #5539, #12280, #9825 ) ;
#6246=CARTESIAN_POINT ( 'NONE',  ( 1.999999999999998668, 0.000000000000000000, -10.20000000000000107 ) ) ;
#6250=LINE ( 'NONE', #10683, #616 ) ;
#6283=EDGE_LOOP ( 'NONE', ( #9335, #10813, #11356, #4817 ) ) ;
#6314=PRODUCT_DEFINITION ( 'UNKNOWN', '', #9808, #3039 ) ;
#6367=ORIENTED_EDGE ( 'NONE', *, *, #8242, .F. ) ;
#6376=AXIS2_PLACEMENT_3D ( 'NONE', #10264, #154, #292 ) ;
#6453=EDGE_CURVE ( 'NONE', #566, #6215, #5032, .T. ) ;
#6480=CARTESIAN_POINT ( 'NONE',  ( 1.799999999999996048, 1.236893267138826416E-15, 9.999999999999994671 ) ) ;
#6555=( GEOMETRIC_REPRESENTATION_CONTEXT ( 3 ) GLOBAL_UNCERTAINTY_ASSIGNED_CONTEXT ( ( #9589 ) ) GLOBAL_UNIT_ASSIGNED_CONTEXT ( ( #13225, #4524, #13356 ) ) REPRESENTATION_CONTEXT ( 'NONE', 'WORKASPACE' ) );
#6580=CARTESIAN_POINT ( 'NONE',  ( 1.800000000000002931, 0.000000000000000000, 0.000000000000000000 ) ) ;
#6609=ORIENTED_EDGE ( 'NONE', *, *, #7469, .F. ) ;
#6624=CIRCLE ( 'NONE', #14023, 9.999999999999994671 ) ;
#6632=CARTESIAN_POINT ( 'NONE',  ( -1.999999999999998224, 0.000000000000000000, 0.000000000000000000 ) ) ;
#6645=CIRCLE ( 'NONE', #10579, 13.29999999999999893 ) ;
#6653=CARTESIAN_POINT ( 'NONE',  ( 2.000000000000001776, 0.000000000000000000, 0.000000000000000000 ) ) ;
#6664=TOROIDAL_SURFACE ( 'NONE', #9649, 11.75000000000000000, 1.050000000000000266 ) ;
#6675=EDGE_CURVE ( 'NONE', #4963, #5710, #12856, .T. ) ;
#6678=CARTESIAN_POINT ( 'NONE',  ( -20.63749999999999929, 0.000000000000000000, 0.000000000000000000 ) ) ;
#6697=CARTESIAN_POINT ( 'NONE',  ( 0.2277608394786177770, 0.000000000000000000, 0.000000000000000000 ) ) ;
#6744=CARTESIAN_POINT ( 'NONE',  ( -1.999999999999998224, 0.000000000000000000, 0.000000000000000000 ) ) ;
#6822=AXIS2_PLACEMENT_3D ( 'NONE', #14002, #7266, #7125 ) ;
#6836=AXIS2_PLACEMENT_3D ( 'NONE', #1330, #3460, #2364 ) ;
#6848=EDGE_CURVE ( 'NONE', #4302, #9549, #12174, .T. ) ;
#6886=VECTOR ( 'NONE', #10522, 1000.000000000000000 ) ;
#6919=DIRECTION ( 'NONE',  ( 0.000000000000000000, 0.000000000000000000, -1.000000000000000000 ) ) ;
#6941=FACE_OUTER_BOUND ( 'NONE', #2873, .T. ) ;
#6942=EDGE_LOOP ( 'NONE', ( #8407, #9013, #10337, #10470 ) ) ;
#6945=EDGE_LOOP ( 'NONE', ( #2076, #8794, #5225, #10011 ) ) ;
#6949=CIRCLE ( 'NONE', #11825, 13.50000000000000178 ) ;
#6985=CARTESIAN_POINT ( 'NONE',  ( 0.7826237921249276086, 1.524685264938454646E-15, -12.44999999999999929 ) ) ;
#6987=DIRECTION ( 'NONE',  ( 0.000000000000000000, 0.000000000000000000, -1.000000000000000000 ) ) ;
#6992=CARTESIAN_POINT ( 'NONE',  ( -1.800000000000002931, 0.000000000000000000, 0.000000000000000000 ) ) ;
#6995=CIRCLE ( 'NONE', #7684, 11.05000000000000071 ) ;
#7005=AXIS2_PLACEMENT_3D ( 'NONE', #10360, #4931, #9494 ) ;
#7040=ORIENTED_EDGE ( 'NONE', *, *, #2443, .F. ) ;
#7052=VERTEX_POINT ( 'NONE', #10301 ) ;
#7069=DIRECTION ( 'NONE',  ( 0.000000000000000000, 0.000000000000000000, -1.000000000000000000 ) ) ;
#7072=ORIENTED_EDGE ( 'NONE', *, *, #13006, .T. ) ;
#7100=CIRCLE ( 'NONE', #13116, 10.20000000000000107 ) ;
#7106=ORIENTED_EDGE ( 'NONE', *, *, #10859, .F. ) ;
#7125=DIRECTION ( 'NONE',  ( 0.000000000000000000, 0.000000000000000000, -1.000000000000000000 ) ) ;
#7189=EDGE_CURVE ( 'NONE', #3295, #5615, #576, .T. ) ;
#7190=ORIENTED_EDGE ( 'NONE', *, *, #8242, .T. ) ;
#7221=CARTESIAN_POINT ( 'NONE',  ( -0.7826237921249277196, 0.000000000000000000, -11.05000000000000071 ) ) ;
#7239=CARTESIAN_POINT ( 'NONE',  ( 1.800000000000001155, 0.000000000000000000, 0.000000000000000000 ) ) ;
#7241=CARTESIAN_POINT ( 'NONE',  ( -2.000000000000000888, 12.77500000000000036, 0.000000000000000000 ) ) ;
#7253=VERTEX_POINT ( 'NONE', #11971 ) ;
#7266=DIRECTION ( 'NONE',  ( 0.000000000000000000, -1.000000000000000000, 0.000000000000000000 ) ) ;
#7285=DIRECTION ( 'NONE',  ( 1.000000000000000000, 0.000000000000000000, 0.000000000000000000 ) ) ;
#7307=CIRCLE ( 'NONE', #324, 11.05000000000000071 ) ;
#7315=CARTESIAN_POINT ( 'NONE',  ( 1.800000000000002931, 0.000000000000000000, 0.000000000000000000 ) ) ;
#7317=ADVANCED_BREP_SHAPE_REPRESENTATION ( '', ( #8329, #14039 ), #11646 ) ;
#7321=VERTEX_POINT ( 'NONE', #3351 ) ;
#7353=ORIENTED_EDGE ( 'NONE', *, *, #5607, .T. ) ;
#7373=EDGE_CURVE ( 'NONE', #14164, #12252, #12187, .T. ) ;
#7386=ADVANCED_FACE ( 'NONE', ( #13469, #3551 ), #11027, .T. ) ;
#7402=DIRECTION ( 'NONE',  ( 1.000000000000000000, 0.000000000000000000, 0.000000000000000000 ) ) ;
#7411=ORIENTED_EDGE ( 'NONE', *, *, #603, .T. ) ;
#7450=DIRECTION ( 'NONE',  ( 1.000000000000000000, 0.000000000000000000, 0.000000000000000000 ) ) ;
#7469=EDGE_CURVE ( 'NONE', #2766, #11206, #4548, .T. ) ;
#7471=ADVANCED_FACE ( 'NONE', ( #6149 ), #1751, .T. ) ;
#7547=EDGE_LOOP ( 'NONE', ( #12198, #9882, #7775, #4190 ) ) ;
#7684=AXIS2_PLACEMENT_3D ( 'NONE', #6744, #1433, #3618 ) ;
#7690=ORIENTED_EDGE ( 'NONE', *, *, #11720, .F. ) ;
#7713=DIRECTION ( 'NONE',  ( 1.000000000000000000, 0.000000000000000000, 0.000000000000000000 ) ) ;
#7742=DIRECTION ( 'NONE',  ( 0.000000000000000000, 0.000000000000000000, -1.000000000000000000 ) ) ;
#7768=( NAMED_UNIT ( * ) SI_UNIT ( $, .STERADIAN. ) SOLID_ANGLE_UNIT ( ) );
#7772=CIRCLE ( 'NONE', #1506, 0.2000000000000022593 ) ;
#7775=ORIENTED_EDGE ( 'NONE', *, *, #758, .T. ) ;
#7785=FACE_OUTER_BOUND ( 'NONE', #1148, .T. ) ;
#7805=EDGE_CURVE ( 'NONE', #5615, #3295, #14045, .T. ) ;
#7807=ORIENTED_EDGE ( 'NONE', *, *, #10581, .T. ) ;
#7808=CIRCLE ( 'NONE', #13600, 0.2000000000000022593 ) ;
#7821=EDGE_CURVE ( 'NONE', #12252, #10809, #8736, .T. ) ;
#7836=CARTESIAN_POINT ( 'NONE',  ( -20.63749999999999574, 1.524685264938454646E-15, 12.44999999999999929 ) ) ;
#7843=SHAPE_REPRESENTATION_RELATIONSHIP ( 'NONE' , 'NONE' ,  #208, #7317 ) ;
#7881=DIRECTION ( 'NONE',  ( 1.000000000000000000, 0.000000000000000000, 0.000000000000000000 ) ) ;
#7887=DIRECTION ( 'NONE',  ( 0.000000000000000000, 0.000000000000000000, -1.000000000000000000 ) ) ;
#7906=DIRECTION ( 'NONE',  ( 0.000000000000000000, 0.000000000000000000, 1.000000000000000000 ) ) ;
#7914=ORIENTED_EDGE ( 'NONE', *, *, #7373, .F. ) ;
#7918=DIRECTION ( 'NONE',  ( 0.000000000000000000, 0.000000000000000000, -1.000000000000000000 ) ) ;
#7922=DIRECTION ( 'NONE',  ( 0.000000000000000000, 0.000000000000000000, -1.000000000000000000 ) ) ;
#7925=AXIS2_PLACEMENT_3D ( 'NONE', #811, #9696, #14103 ) ;
#7947=EDGE_LOOP ( 'NONE', ( #8724, #6037, #4135, #4600 ) ) ;
#7953=FACE_OUTER_BOUND ( 'NONE', #11758, .T. ) ;
#7970=ORIENTED_EDGE ( 'NONE', *, *, #7805, .F. ) ;
#7990=VECTOR ( 'NONE', #2445, 1000.000000000000000 ) ;
#7996=DIRECTION ( 'NONE',  ( 0.000000000000000000, 0.000000000000000000, -1.000000000000000000 ) ) ;
#8003=CARTESIAN_POINT ( 'NONE',  ( -20.63749999999999929, 0.000000000000000000, 0.000000000000000000 ) ) ;
#8015=CARTESIAN_POINT ( 'NONE',  ( 1.799999999999996048, 0.000000000000000000, 0.000000000000000000 ) ) ;
#8021=AXIS2_PLACEMENT_3D ( 'NONE', #1303, #9297, #3784 ) ;
#8064=ORIENTED_EDGE ( 'NONE', *, *, #2589, .T. ) ;
#8068=CARTESIAN_POINT ( 'NONE',  ( 0.7826237921249277196, 0.000000000000000000, 0.000000000000000000 ) ) ;
#8077=DIRECTION ( 'NONE',  ( 0.000000000000000000, 0.000000000000000000, -1.000000000000000000 ) ) ;
#8100=CARTESIAN_POINT ( 'NONE',  ( -1.800000000000001155, 0.000000000000000000, 0.000000000000000000 ) ) ;
#8119=ORIENTED_EDGE ( 'NONE', *, *, #603, .F. ) ;
#8135=AXIS2_PLACEMENT_3D ( 'NONE', #6992, #11425, #1467 ) ;
#8169=DIRECTION ( 'NONE',  ( -1.000000000000000000, 0.000000000000000000, -0.000000000000000000 ) ) ;
#8198=PRODUCT_CONTEXT ( 'NONE', #11561, 'mechanical' ) ;
#8217=ORIENTED_EDGE ( 'NONE', *, *, #4935, .F. ) ;
#8242=EDGE_CURVE ( 'NONE', #14164, #7052, #14281, .T. ) ;
#8243=PLANE ( 'NONE',  #2806 ) ;
#8255=ORIENTED_EDGE ( 'NONE', *, *, #12515, .T. ) ;
#8258=EDGE_CURVE ( 'NONE', #9549, #13517, #12348, .T. ) ;
#8271=DIRECTION ( 'NONE',  ( 0.000000000000000000, 0.000000000000000000, -1.000000000000000000 ) ) ;
#8285=ORIENTED_EDGE ( 'NONE', *, *, #5492, .T. ) ;
#8316=FACE_OUTER_BOUND ( 'NONE', #11716, .T. ) ;
#8323=FACE_OUTER_BOUND ( 'NONE', #4140, .T. ) ;
#8329=MANIFOLD_SOLID_BREP ( 'OuterRace', #10537 ) ;
#8345=SHAPE_DEFINITION_REPRESENTATION ( #1232, #208 ) ;
#8391=ADVANCED_FACE ( 'NONE', ( #640 ), #1784, .T. ) ;
#8407=ORIENTED_EDGE ( 'NONE', *, *, #6453, .F. ) ;
#8411=DIRECTION ( 'NONE',  ( 0.000000000000000000, 0.000000000000000000, 1.000000000000000000 ) ) ;
#8443=FACE_OUTER_BOUND ( 'NONE', #2260, .T. ) ;
#8506=VECTOR ( 'NONE', #3436, 1000.000000000000000 ) ;
#8513=TOROIDAL_SURFACE ( 'NONE', #9687, 10.20000000000000107, 0.2000000000000031197 ) ;
#8522=ADVANCED_FACE ( 'NONE', ( #7953 ), #8513, .T. ) ;
#8582=DIRECTION ( 'NONE',  ( 0.000000000000000000, 0.000000000000000000, -1.000000000000000000 ) ) ;
#8601=DIRECTION ( 'NONE',  ( 0.000000000000000000, 0.000000000000000000, -1.000000000000000000 ) ) ;
#8629=DIRECTION ( 'NONE',  ( 0.000000000000000000, 0.000000000000000000, -1.000000000000000000 ) ) ;
#8696=CYLINDRICAL_SURFACE ( 'NONE', #1615, 12.44999999999999929 ) ;
#8724=ORIENTED_EDGE ( 'NONE', *, *, #1737, .T. ) ;
#8725=DIRECTION ( 'NONE',  ( 1.000000000000000000, 0.000000000000000000, 0.000000000000000000 ) ) ;
#8727=DIRECTION ( 'NONE',  ( 1.000000000000000000, 0.000000000000000000, 0.000000000000000000 ) ) ;
#8736=CIRCLE ( 'NONE', #5709, 12.44999999999999929 ) ;
#8794=ORIENTED_EDGE ( 'NONE', *, *, #3577, .T. ) ;
#8799=CARTESIAN_POINT ( 'NONE',  ( -0.7826237921249277196, 0.000000000000000000, 0.000000000000000000 ) ) ;
#8804=( NAMED_UNIT ( * ) SI_UNIT ( $, .STERADIAN. ) SOLID_ANGLE_UNIT ( ) );
#8810=AXIS2_PLACEMENT_3D ( 'NONE', #12413, #11407, #1519 ) ;
#8835=FACE_OUTER_BOUND ( 'NONE', #5597, .T. ) ;
#8839=DIRECTION ( 'NONE',  ( 0.000000000000000000, 1.224646799147361589E-16, 1.000000000000000000 ) ) ;
#8895=CARTESIAN_POINT ( 'NONE',  ( -0.2277608394786177770, 1.564486285910743648E-15, -12.77499999999999858 ) ) ;
#8901=ADVANCED_FACE ( 'NONE', ( #233 ), #1049, .T. ) ;
#8951=CARTESIAN_POINT ( 'NONE',  ( -2.000000000000001776, 0.000000000000000000, 0.000000000000000000 ) ) ;
#8965=VECTOR ( 'NONE', #11128, 1000.000000000000000 ) ;
#8990=CARTESIAN_POINT ( 'NONE',  ( 0.7826237921249277196, 0.000000000000000000, 0.000000000000000000 ) ) ;
#9012=DIRECTION ( 'NONE',  ( 1.000000000000000000, 0.000000000000000000, 0.000000000000000000 ) ) ;
#9013=ORIENTED_EDGE ( 'NONE', *, *, #3644, .T. ) ;
#9032=AXIS2_PLACEMENT_3D ( 'NONE', #10958, #14203, #8629 ) ;
#9034=CARTESIAN_POINT ( 'NONE',  ( 1.799999999999996048, 1.249139735130300365E-15, 10.20000000000000107 ) ) ;
#9058=EDGE_CURVE ( 'NONE', #14164, #3772, #2588, .T. ) ;
#9071=VERTEX_POINT ( 'NONE', #10496 ) ;
#9090=ORIENTED_EDGE ( 'NONE', *, *, #9578, .F. ) ;
#9096=CIRCLE ( 'NONE', #10732, 10.72500000000000142 ) ;
#9112=VERTEX_POINT ( 'NONE', #7221 ) ;
#9236=ORIENTED_EDGE ( 'NONE', *, *, #12004, .F. ) ;
#9238=ORIENTED_EDGE ( 'NONE', *, *, #765, .T. ) ;
#9254=FACE_OUTER_BOUND ( 'NONE', #2158, .T. ) ;
#9286=EDGE_LOOP ( 'NONE', ( #984, #12419, #7807, #13217 ) ) ;
#9297=DIRECTION ( 'NONE',  ( -1.000000000000000000, -0.000000000000000000, -0.000000000000000000 ) ) ;
#9308=ORIENTED_EDGE ( 'NONE', *, *, #14016, .F. ) ;
#9316=ADVANCED_FACE ( 'NONE', ( #7785 ), #13443, .F. ) ;
#9335=ORIENTED_EDGE ( 'NONE', *, *, #8258, .F. ) ;
#9348=DIRECTION ( 'NONE',  ( 1.000000000000000000, 0.000000000000000000, 0.000000000000000000 ) ) ;
#9351=DIRECTION ( 'NONE',  ( 0.000000000000000000, 0.000000000000000000, -1.000000000000000000 ) ) ;
#9361=ORIENTED_EDGE ( 'NONE', *, *, #2960, .T. ) ;
#9397=CARTESIAN_POINT ( 'NONE',  ( -2.000000000000001776, 0.000000000000000000, 0.000000000000000000 ) ) ;
#9418=DIRECTION ( 'NONE',  ( 0.000000000000000000, 0.000000000000000000, 1.000000000000000000 ) ) ;
#9435=VECTOR ( 'NONE', #3946, 1000.000000000000000 ) ;
#9437=LINE ( 'NONE', #5167, #6886 ) ;
#9494=DIRECTION ( 'NONE',  ( 0.000000000000000000, 0.000000000000000000, 1.000000000000000000 ) ) ;
#9523=ORIENTED_EDGE ( 'NONE', *, *, #7189, .T. ) ;
#9540=AXIS2_PLACEMENT_3D ( 'NONE', #5540, #9967, #11263 ) ;
#9549=VERTEX_POINT ( 'NONE', #1327 ) ;
#9578=EDGE_CURVE ( 'NONE', #4230, #2417, #4461, .T. ) ;
#9589=UNCERTAINTY_MEASURE_WITH_UNIT (LENGTH_MEASURE( 1.000000000000000082E-05 ), #13225, 'distance_accuracy_value', 'NONE');
#9632=DIRECTION ( 'NONE',  ( 0.000000000000000000, 0.000000000000000000, -1.000000000000000000 ) ) ;
#9638=TOROIDAL_SURFACE ( 'NONE', #3392, 10.20000000000000107, 0.2000000000000031197 ) ;
#9649=AXIS2_PLACEMENT_3D ( 'NONE', #1812, #637, #8411 ) ;
#9687=AXIS2_PLACEMENT_3D ( 'NONE', #2390, #4432, #13333 ) ;
#9696=DIRECTION ( 'NONE',  ( 1.000000000000000000, 0.000000000000000000, 0.000000000000000000 ) ) ;
#9716=CIRCLE ( 'NONE', #6226, 0.2000000000000022593 ) ;
#9729=AXIS2_PLACEMENT_3D ( 'NONE', #2591, #5776, #3604 ) ;
#9762=EDGE_CURVE ( 'NONE', #7321, #4963, #6995, .T. ) ;
#9808=PRODUCT_DEFINITION_FORMATION_WITH_SPECIFIED_SOURCE ( 'ANY', '', #3229, .NOT_KNOWN. ) ;
#9825=DIRECTION ( 'NONE',  ( 0.000000000000000000, 1.224646799147351975E-16, 1.000000000000000000 ) ) ;
#9838=EDGE_CURVE ( 'NONE', #10809, #12252, #6065, .T. ) ;
#9862=AXIS2_PLACEMENT_3D ( 'NONE', #1907, #8725, #4160 ) ;
#9864=ORIENTED_EDGE ( 'NONE', *, *, #2443, .T. ) ;
#9875=AXIS2_PLACEMENT_3D ( 'NONE', #8100, #3613, #9351 ) ;
#9882=ORIENTED_EDGE ( 'NONE', *, *, #8258, .T. ) ;
#9891=ADVANCED_FACE ( 'NONE', ( #46 ), #12393, .T. ) ;
#9905=DIRECTION ( 'NONE',  ( 1.000000000000000000, 0.000000000000000000, 0.000000000000000000 ) ) ;
#9908=VECTOR ( 'NONE', #2131, 1000.000000000000000 ) ;
#9967=DIRECTION ( 'NONE',  ( 1.000000000000000000, 0.000000000000000000, 0.000000000000000000 ) ) ;
#9970=DIRECTION ( 'NONE',  ( 1.000000000000000000, 0.000000000000000000, 0.000000000000000000 ) ) ;
#9991=CARTESIAN_POINT ( 'NONE',  ( 0.000000000000000000, 0.000000000000000000, 0.000000000000000000 ) ) ;
#10008=ADVANCED_FACE ( 'NONE', ( #8323 ), #10480, .T. ) ;
#10011=ORIENTED_EDGE ( 'NONE', *, *, #5095, .F. ) ;
#10012=CARTESIAN_POINT ( 'NONE',  ( 0.000000000000000000, 1.438959988998140160E-15, -11.75000000000000000 ) ) ;
#10015=CARTESIAN_POINT ( 'NONE',  ( 1.800000000000002931, 0.000000000000000000, -13.50000000000000178 ) ) ;
#10053=CARTESIAN_POINT ( 'NONE',  ( 1.799999999999996048, 0.000000000000000000, -10.20000000000000107 ) ) ;
#10065=ADVANCED_FACE ( 'NONE', ( #9254 ), #368, .T. ) ;
#10095=DIRECTION ( 'NONE',  ( -1.000000000000000000, -0.000000000000000000, -0.000000000000000000 ) ) ;
#10209=DIRECTION ( 'NONE',  ( 1.000000000000000000, 0.000000000000000000, 0.000000000000000000 ) ) ;
#10228=EDGE_LOOP ( 'NONE', ( #987, #13966, #4599, #7411 ) ) ;
#10264=CARTESIAN_POINT ( 'NONE',  ( -1.799999999999996048, 0.000000000000000000, 0.000000000000000000 ) ) ;
#10301=CARTESIAN_POINT ( 'NONE',  ( 0.2277608394786177770, 0.000000000000000000, 10.72500000000000142 ) ) ;
#10309=CARTESIAN_POINT ( 'NONE',  ( 2.000000000000001776, 1.524685264938454646E-15, 12.44999999999999929 ) ) ;
#10312=ADVANCED_FACE ( 'NONE', ( #8443 ), #1623, .T. ) ;
#10337=ORIENTED_EDGE ( 'NONE', *, *, #13959, .F. ) ;
#10351=CARTESIAN_POINT ( 'NONE',  ( 1.999999999999997335, 10.20000000000000107, 0.000000000000000000 ) ) ;
#10354=DIRECTION ( 'NONE',  ( 1.000000000000000000, 0.000000000000000000, 0.000000000000000000 ) ) ;
#10358=DIRECTION ( 'NONE',  ( 0.000000000000000000, -1.224646799147352468E-16, 1.000000000000000000 ) ) ;
#10360=CARTESIAN_POINT ( 'NONE',  ( 0.000000000000000000, 0.000000000000000000, 0.000000000000000000 ) ) ;
#10410=ORIENTED_EDGE ( 'NONE', *, *, #5826, .T. ) ;
#10428=ADVANCED_FACE ( 'NONE', ( #4318 ), #497, .T. ) ;
#10469=DIRECTION ( 'NONE',  ( 0.000000000000000000, 0.000000000000000000, -1.000000000000000000 ) ) ;
#10470=ORIENTED_EDGE ( 'NONE', *, *, #5826, .F. ) ;
#10480=TOROIDAL_SURFACE ( 'NONE', #7005, 11.75000000000000000, 1.050000000000000266 ) ;
#10487=ADVANCED_FACE ( 'NONE', ( #11647 ), #14021, .F. ) ;
#10491=CARTESIAN_POINT ( 'NONE',  ( -20.63749999999999929, 0.000000000000000000, 0.000000000000000000 ) ) ;
#10496=CARTESIAN_POINT ( 'NONE',  ( -0.2277608394786177770, 0.000000000000000000, 12.77499999999999858 ) ) ;
#10506=ORIENTED_EDGE ( 'NONE', *, *, #14016, .T. ) ;
#10508=CARTESIAN_POINT ( 'NONE',  ( 0.000000000000000000, 0.000000000000000000, 0.000000000000000000 ) ) ;
#10522=DIRECTION ( 'NONE',  ( 1.000000000000000000, 0.000000000000000000, 0.000000000000000000 ) ) ;
#10537=CLOSED_SHELL ( 'NONE', ( #10428, #10755, #8391, #2400, #1961, #12965, #785, #3018, #4612, #10312, #9891, #14056, #10008, #10065, #3826, #11285, #8522, #10487, #8901, #11357, #5262, #9316, #4510, #7471, #13585, #1679, #7386, #3303 ) ) ;
#10541=ORIENTED_EDGE ( 'NONE', *, *, #1089, .T. ) ;
#10551=CARTESIAN_POINT ( 'NONE',  ( 0.000000000000000000, 0.000000000000000000, 0.000000000000000000 ) ) ;
#10564=CARTESIAN_POINT ( 'NONE',  ( -20.63749999999999929, 0.000000000000000000, -10.72500000000000142 ) ) ;
#10566=AXIS2_PLACEMENT_3D ( 'NONE', #4215, #4283, #14274 ) ;
#10575=DIRECTION ( 'NONE',  ( 0.000000000000000000, 0.000000000000000000, -1.000000000000000000 ) ) ;
#10579=AXIS2_PLACEMENT_3D ( 'NONE', #1388, #2711, #10469 ) ;
#10581=EDGE_CURVE ( 'NONE', #4302, #4187, #3541, .T. ) ;
#10595=AXIS2_PLACEMENT_3D ( 'NONE', #656, #2048, #8582 ) ;
#10676=VERTEX_POINT ( 'NONE', #1099 ) ;
#10683=CARTESIAN_POINT ( 'NONE',  ( -20.63749999999999574, 0.000000000000000000, -12.77499999999999858 ) ) ;
#10717=AXIS2_PLACEMENT_3D ( 'NONE', #8990, #185, #11172 ) ;
#10732=AXIS2_PLACEMENT_3D ( 'NONE', #2757, #3919, #5090 ) ;
#10745=ORIENTED_EDGE ( 'NONE', *, *, #7189, .F. ) ;
#10755=ADVANCED_FACE ( 'NONE', ( #10919 ), #3165, .T. ) ;
#10809=VERTEX_POINT ( 'NONE', #13436 ) ;
#10813=ORIENTED_EDGE ( 'NONE', *, *, #6848, .F. ) ;
#10859=EDGE_CURVE ( 'NONE', #1275, #4230, #14197, .T. ) ;
#10864=LINE ( 'NONE', #888, #5779 ) ;
#10876=CARTESIAN_POINT ( 'NONE',  ( -1.799999999999996048, 0.000000000000000000, -9.999999999999998224 ) ) ;
#10879=EDGE_CURVE ( 'NONE', #2998, #12823, #13733, .T. ) ;
#10894=FACE_OUTER_BOUND ( 'NONE', #7547, .T. ) ;
#10913=AXIS2_PLACEMENT_3D ( 'NONE', #12744, #8169, #1420 ) ;
#10919=FACE_OUTER_BOUND ( 'NONE', #2222, .T. ) ;
#10953=ORIENTED_EDGE ( 'NONE', *, *, #9762, .T. ) ;
#10958=CARTESIAN_POINT ( 'NONE',  ( 0.000000000000000000, 0.000000000000000000, 11.75000000000000000 ) ) ;
#11027=PLANE ( 'NONE',  #13111 ) ;
#11088=EDGE_LOOP ( 'NONE', ( #13775, #13870, #3928, #12611 ) ) ;
#11089=DIRECTION ( 'NONE',  ( 1.000000000000000000, 0.000000000000000000, 0.000000000000000000 ) ) ;
#11091=DIRECTION ( 'NONE',  ( 1.000000000000000000, 0.000000000000000000, 0.000000000000000000 ) ) ;
#11111=CARTESIAN_POINT ( 'NONE',  ( -2.000000000000001776, 0.000000000000000000, -12.77500000000000036 ) ) ;
#11128=DIRECTION ( 'NONE',  ( 1.000000000000000000, 0.000000000000000000, 0.000000000000000000 ) ) ;
#11131=DIRECTION ( 'NONE',  ( 0.000000000000000000, 0.000000000000000000, -1.000000000000000000 ) ) ;
#11144=DIRECTION ( 'NONE',  ( 1.000000000000000000, 0.000000000000000000, 0.000000000000000000 ) ) ;
#11146=ORIENTED_EDGE ( 'NONE', *, *, #1089, .F. ) ;
#11148=AXIS2_PLACEMENT_3D ( 'NONE', #10053, #3802, #6919 ) ;
#11151=DIRECTION ( 'NONE',  ( 0.000000000000000000, 1.224646799147361589E-16, 1.000000000000000000 ) ) ;
#11172=DIRECTION ( 'NONE',  ( 0.000000000000000000, 0.000000000000000000, 1.000000000000000000 ) ) ;
#11190=DIRECTION ( 'NONE',  ( 0.000000000000000000, 0.000000000000000000, -1.000000000000000000 ) ) ;
#11198=( LENGTH_UNIT ( ) NAMED_UNIT ( * ) SI_UNIT ( .MILLI., .METRE. ) );
#11206=VERTEX_POINT ( 'NONE', #2384 ) ;
#11213=DIRECTION ( 'NONE',  ( 1.000000000000000000, 0.000000000000000000, 0.000000000000000000 ) ) ;
#11216=CARTESIAN_POINT ( 'NONE',  ( 2.000000000000001776, 1.641026710857453312E-15, 13.29999999999999893 ) ) ;
#11230=CARTESIAN_POINT ( 'NONE',  ( -1.799999999999996048, 1.249139735130300365E-15, 10.20000000000000107 ) ) ;
#11263=DIRECTION ( 'NONE',  ( 0.000000000000000000, 0.000000000000000000, -1.000000000000000000 ) ) ;
#11285=ADVANCED_FACE ( 'NONE', ( #13610, #2744 ), #11663, .T. ) ;
#11289=EDGE_CURVE ( 'NONE', #11206, #2766, #14166, .T. ) ;
#11332=EDGE_LOOP ( 'NONE', ( #10745, #7970 ) ) ;
#11335=SURFACE_SIDE_STYLE ('',( #1165 ) ) ;
#11347=DIRECTION ( 'NONE',  ( 1.000000000000000000, 0.000000000000000000, 0.000000000000000000 ) ) ;
#11353=DIRECTION ( 'NONE',  ( 0.000000000000000000, -1.000000000000000000, 0.000000000000000000 ) ) ;
#11356=ORIENTED_EDGE ( 'NONE', *, *, #5427, .T. ) ;
#11357=ADVANCED_FACE ( 'NONE', ( #3901, #8316 ), #2527, .T. ) ;
#11407=DIRECTION ( 'NONE',  ( 1.000000000000000000, 0.000000000000000000, 0.000000000000000000 ) ) ;
#11425=DIRECTION ( 'NONE',  ( 1.000000000000000000, 0.000000000000000000, 0.000000000000000000 ) ) ;
#11461=EDGE_CURVE ( 'NONE', #5968, #4187, #2110, .T. ) ;
#11464=CIRCLE ( 'NONE', #84, 10.72499999999999964 ) ;
#11493=CARTESIAN_POINT ( 'NONE',  ( -1.800000000000002931, 1.653273178848927064E-15, 13.50000000000000355 ) ) ;
#11505=AXIS2_PLACEMENT_3D ( 'NONE', #6653, #11089, #5833 ) ;
#11561=APPLICATION_CONTEXT ( 'automotive_design' ) ;
#11584=EDGE_LOOP ( 'NONE', ( #3074, #11722, #4714, #3327 ) ) ;
#11587=DIRECTION ( 'NONE',  ( 0.000000000000000000, 0.000000000000000000, -1.000000000000000000 ) ) ;
#11589=ORIENTED_EDGE ( 'NONE', *, *, #4868, .T. ) ;
#11646=( GEOMETRIC_REPRESENTATION_CONTEXT ( 3 ) GLOBAL_UNCERTAINTY_ASSIGNED_CONTEXT ( ( #708 ) ) GLOBAL_UNIT_ASSIGNED_CONTEXT ( ( #11198, #5672, #8804 ) ) REPRESENTATION_CONTEXT ( 'NONE', 'WORKASPACE' ) );
#11647=FACE_OUTER_BOUND ( 'NONE', #6283, .T. ) ;
#11663=PLANE ( 'NONE',  #6067 ) ;
#11666=DIRECTION ( 'NONE',  ( 0.000000000000000000, 0.000000000000000000, -1.000000000000000000 ) ) ;
#11716=EDGE_LOOP ( 'NONE', ( #5033, #9308 ) ) ;
#11720=EDGE_CURVE ( 'NONE', #1275, #10676, #923, .T. ) ;
#11722=ORIENTED_EDGE ( 'NONE', *, *, #4935, .T. ) ;
#11724=AXIS2_PLACEMENT_3D ( 'NONE', #10012, #3480, #4430 ) ;
#11752=DIRECTION ( 'NONE',  ( 0.000000000000000000, 0.000000000000000000, -1.000000000000000000 ) ) ;
#11758=EDGE_LOOP ( 'NONE', ( #5450, #11915, #12999, #3824 ) ) ;
#11768=CARTESIAN_POINT ( 'NONE',  ( -0.7826237921249277196, 1.353234713057825478E-15, 11.05000000000000071 ) ) ;
#11784=DIRECTION ( 'NONE',  ( 0.000000000000000000, 1.000000000000000000, -1.224646799147353207E-16 ) ) ;
#11789=EDGE_LOOP ( 'NONE', ( #4945, #7072, #2951, #5753 ) ) ;
#11790=CARTESIAN_POINT ( 'NONE',  ( -1.799999999999996048, 0.000000000000000000, -10.20000000000000107 ) ) ;
#11798=CARTESIAN_POINT ( 'NONE',  ( 2.000000000000001776, 0.000000000000000000, 0.000000000000000000 ) ) ;
#11813=CIRCLE ( 'NONE', #1105, 0.2000000000000022593 ) ;
#11825=AXIS2_PLACEMENT_3D ( 'NONE', #6580, #7450, #11880 ) ;
#11880=DIRECTION ( 'NONE',  ( 0.000000000000000000, 0.000000000000000000, -1.000000000000000000 ) ) ;
#11915=ORIENTED_EDGE ( 'NONE', *, *, #11289, .T. ) ;
#11964=AXIS2_PLACEMENT_3D ( 'NONE', #2820, #10354, #2747 ) ;
#11971=CARTESIAN_POINT ( 'NONE',  ( 1.799999999999996048, 0.000000000000000000, -9.999999999999994671 ) ) ;
#11982=CIRCLE ( 'NONE', #6188, 12.77499999999999858 ) ;
#11990=VERTEX_POINT ( 'NONE', #5271 ) ;
#12003=VECTOR ( 'NONE', #9012, 1000.000000000000000 ) ;
#12004=EDGE_CURVE ( 'NONE', #4187, #5968, #7100, .T. ) ;
#12005=DIRECTION ( 'NONE',  ( 1.000000000000000000, 0.000000000000000000, 0.000000000000000000 ) ) ;
#12052=CARTESIAN_POINT ( 'NONE',  ( -20.63749999999999929, 0.000000000000000000, 0.000000000000000000 ) ) ;
#12074=LINE ( 'NONE', #14161, #9908 ) ;
#12131=CARTESIAN_POINT ( 'NONE',  ( -0.2277608394786177770, 0.000000000000000000, 0.000000000000000000 ) ) ;
#12160=EDGE_LOOP ( 'NONE', ( #12458, #11589 ) ) ;
#12168=EDGE_CURVE ( 'NONE', #11990, #5253, #6645, .T. ) ;
#12174=CIRCLE ( 'NONE', #9862, 9.999999999999998224 ) ;
#12187=CIRCLE ( 'NONE', #11724, 1.050000000000000488 ) ;
#12198=ORIENTED_EDGE ( 'NONE', *, *, #2380, .F. ) ;
#12227=AXIS2_PLACEMENT_3D ( 'NONE', #13059, #7402, #3134 ) ;
#12248=VERTEX_POINT ( 'NONE', #3867 ) ;
#12252=VERTEX_POINT ( 'NONE', #6985 ) ;
#12280=DIRECTION ( 'NONE',  ( 0.000000000000000000, 1.000000000000000000, -1.224646799147353207E-16 ) ) ;
#12289=CARTESIAN_POINT ( 'NONE',  ( -20.63749999999999574, 0.000000000000000000, 0.000000000000000000 ) ) ;
#12300=FACE_OUTER_BOUND ( 'NONE', #6942, .T. ) ;
#12308=DIRECTION ( 'NONE',  ( 0.000000000000000000, 1.000000000000000000, -1.224646799147353207E-16 ) ) ;
#12310=AXIS2_PLACEMENT_3D ( 'NONE', #2426, #11213, #10 ) ;
#12324=DIRECTION ( 'NONE',  ( 0.000000000000000000, 0.000000000000000000, -1.000000000000000000 ) ) ;
#12348=LINE ( 'NONE', #2409, #8965 ) ;
#12359=ORIENTED_EDGE ( 'NONE', *, *, #1917, .T. ) ;
#12383=CARTESIAN_POINT ( 'NONE',  ( -20.63749999999999574, 0.000000000000000000, -13.50000000000000355 ) ) ;
#12393=CYLINDRICAL_SURFACE ( 'NONE', #3308, 10.72500000000000142 ) ;
#12396=CARTESIAN_POINT ( 'NONE',  ( -1.800000000000002931, 0.000000000000000000, -13.50000000000000355 ) ) ;
#12413=CARTESIAN_POINT ( 'NONE',  ( -20.63749999999999929, 0.000000000000000000, 0.000000000000000000 ) ) ;
#12419=ORIENTED_EDGE ( 'NONE', *, *, #2380, .T. ) ;
#12426=ORIENTED_EDGE ( 'NONE', *, *, #9838, .T. ) ;
#12438=CARTESIAN_POINT ( 'NONE',  ( -20.63749999999999574, 0.000000000000000000, 0.000000000000000000 ) ) ;
#12441=CIRCLE ( 'NONE', #8021, 12.77499999999999858 ) ;
#12446=AXIS2_PLACEMENT_3D ( 'NONE', #6697, #10095, #7906 ) ;
#12458=ORIENTED_EDGE ( 'NONE', *, *, #12168, .T. ) ;
#12512=EDGE_CURVE ( 'NONE', #10809, #5615, #2264, .T. ) ;
#12514=DIRECTION ( 'NONE',  ( 1.000000000000000000, 0.000000000000000000, 0.000000000000000000 ) ) ;
#12515=EDGE_CURVE ( 'NONE', #9071, #5006, #11982, .T. ) ;
#12566=ORIENTED_EDGE ( 'NONE', *, *, #5095, .T. ) ;
#12611=ORIENTED_EDGE ( 'NONE', *, *, #5607, .F. ) ;
#12663=CARTESIAN_POINT ( 'NONE',  ( -1.999999999999998668, 1.249139735130300365E-15, 10.20000000000000107 ) ) ;
#12668=CARTESIAN_POINT ( 'NONE',  ( 1.999999999999998224, 0.000000000000000000, 0.000000000000000000 ) ) ;
#12678=DIRECTION ( 'NONE',  ( -0.000000000000000000, 0.000000000000000000, 1.000000000000000000 ) ) ;
#12691=DIRECTION ( 'NONE',  ( 1.000000000000000000, 0.000000000000000000, 0.000000000000000000 ) ) ;
#12744=CARTESIAN_POINT ( 'NONE',  ( -1.999999999999996669, 11.05000000000000071, 0.000000000000000000 ) ) ;
#12786=ORIENTED_EDGE ( 'NONE', *, *, #2960, .F. ) ;
#12795=CYLINDRICAL_SURFACE ( 'NONE', #10595, 13.50000000000000355 ) ;
#12802=FACE_OUTER_BOUND ( 'NONE', #10228, .T. ) ;
#12811=AXIS2_PLACEMENT_3D ( 'NONE', #6203, #7285, #4172 ) ;
#12823=VERTEX_POINT ( 'NONE', #4946 ) ;
#12852=CARTESIAN_POINT ( 'NONE',  ( -2.000000000000001776, 0.000000000000000000, -13.29999999999999893 ) ) ;
#12856=LINE ( 'NONE', #1750, #9435 ) ;
#12862=CIRCLE ( 'NONE', #6376, 9.999999999999998224 ) ;
#12866=EDGE_CURVE ( 'NONE', #7321, #9112, #9437, .T. ) ;
#12944=EDGE_CURVE ( 'NONE', #6215, #566, #610, .T. ) ;
#12965=ADVANCED_FACE ( 'NONE', ( #846 ), #2493, .T. ) ;
#12984=DIRECTION ( 'NONE',  ( 0.000000000000000000, 0.000000000000000000, -1.000000000000000000 ) ) ;
#12999=ORIENTED_EDGE ( 'NONE', *, *, #3456, .T. ) ;
#13006=EDGE_CURVE ( 'NONE', #11206, #13517, #7808, .T. ) ;
#13059=CARTESIAN_POINT ( 'NONE',  ( -1.999999999999998224, 0.000000000000000000, 0.000000000000000000 ) ) ;
#13062=DIRECTION ( 'NONE',  ( 1.000000000000000000, 0.000000000000000000, 0.000000000000000000 ) ) ;
#13078=DIRECTION ( 'NONE',  ( 0.000000000000000000, 1.224646799147351975E-16, 1.000000000000000000 ) ) ;
#13079=CARTESIAN_POINT ( 'NONE',  ( -2.000000000000001776, 0.000000000000000000, 0.000000000000000000 ) ) ;
#13098=CARTESIAN_POINT ( 'NONE',  ( -1.999999999999998224, 0.000000000000000000, 0.000000000000000000 ) ) ;
#13105=CARTESIAN_POINT ( 'NONE',  ( -20.63749999999999574, 0.000000000000000000, 0.000000000000000000 ) ) ;
#13111=AXIS2_PLACEMENT_3D ( 'NONE', #41, #7881, #12324 ) ;
#13114=CARTESIAN_POINT ( 'NONE',  ( -20.63749999999999574, 0.000000000000000000, 0.000000000000000000 ) ) ;
#13116=AXIS2_PLACEMENT_3D ( 'NONE', #6632, #9905, #7922 ) ;
#13126=CYLINDRICAL_SURFACE ( 'NONE', #3343, 9.999999999999996447 ) ;
#13174=ORIENTED_EDGE ( 'NONE', *, *, #12004, .T. ) ;
#13217=ORIENTED_EDGE ( 'NONE', *, *, #11461, .F. ) ;
#13225=( LENGTH_UNIT ( ) NAMED_UNIT ( * ) SI_UNIT ( .MILLI., .METRE. ) );
#13254=DIRECTION ( 'NONE',  ( 1.000000000000000000, 0.000000000000000000, 0.000000000000000000 ) ) ;
#13263=CARTESIAN_POINT ( 'NONE',  ( -1.799999999999996048, 0.000000000000000000, 0.000000000000000000 ) ) ;
#13265=ORIENTED_EDGE ( 'NONE', *, *, #9058, .T. ) ;
#13267=EDGE_LOOP ( 'NONE', ( #12786, #2859, #3717, #11146 ) ) ;
#13273=DIRECTION ( 'NONE',  ( 0.000000000000000000, 0.000000000000000000, -1.000000000000000000 ) ) ;
#13318=DIRECTION ( 'NONE',  ( 0.000000000000000000, 0.000000000000000000, 1.000000000000000000 ) ) ;
#13333=DIRECTION ( 'NONE',  ( 0.000000000000000000, 0.000000000000000000, -1.000000000000000000 ) ) ;
#13356=( NAMED_UNIT ( * ) SI_UNIT ( $, .STERADIAN. ) SOLID_ANGLE_UNIT ( ) );
#13365=AXIS2_PLACEMENT_3D ( 'NONE', #8799, #8727, #2124 ) ;
#13436=CARTESIAN_POINT ( 'NONE',  ( 0.7826237921249276086, 0.000000000000000000, 12.44999999999999929 ) ) ;
#13443=CYLINDRICAL_SURFACE ( 'NONE', #12310, 12.44999999999999929 ) ;
#13444=CIRCLE ( 'NONE', #14139, 1.050000000000000488 ) ;
#13469=FACE_OUTER_BOUND ( 'NONE', #12160, .T. ) ;
#13489=ORIENTED_EDGE ( 'NONE', *, *, #10879, .F. ) ;
#13517=VERTEX_POINT ( 'NONE', #6480 ) ;
#13554=ORIENTED_EDGE ( 'NONE', *, *, #12512, .F. ) ;
#13559=( NAMED_UNIT ( * ) PLANE_ANGLE_UNIT ( ) SI_UNIT ( $, .RADIAN. ) );
#13585=ADVANCED_FACE ( 'NONE', ( #5195 ), #12795, .T. ) ;
#13588=DIRECTION ( 'NONE',  ( 0.000000000000000000, 0.000000000000000000, -1.000000000000000000 ) ) ;
#13600=AXIS2_PLACEMENT_3D ( 'NONE', #9034, #12308, #11151 ) ;
#13610=FACE_OUTER_BOUND ( 'NONE', #13961, .T. ) ;
#13620=CARTESIAN_POINT ( 'NONE',  ( -1.999999999999998668, 0.000000000000000000, -10.20000000000000107 ) ) ;
#13644=TOROIDAL_SURFACE ( 'NONE', #9729, 10.20000000000000107, 0.2000000000000031197 ) ;
#13681=AXIS2_PLACEMENT_3D ( 'NONE', #1468, #11784, #13078 ) ;
#13733=CIRCLE ( 'NONE', #1922, 13.50000000000000178 ) ;
#13741=EDGE_CURVE ( 'NONE', #9112, #5710, #5285, .T. ) ;
#13761=FACE_OUTER_BOUND ( 'NONE', #3880, .T. ) ;
#13775=ORIENTED_EDGE ( 'NONE', *, *, #9838, .F. ) ;
#13785=CARTESIAN_POINT ( 'NONE',  ( 1.999999999999994893, 0.000000000000000000, -10.72499999999999964 ) ) ;
#13870=ORIENTED_EDGE ( 'NONE', *, *, #12512, .T. ) ;
#13902=DIRECTION ( 'NONE',  ( 1.000000000000000000, 0.000000000000000000, 0.000000000000000000 ) ) ;
#13934=AXIS2_PLACEMENT_3D ( 'NONE', #5956, #3849, #8271 ) ;
#13952=AXIS2_PLACEMENT_3D ( 'NONE', #10491, #2877, #4980 ) ;
#13959=EDGE_CURVE ( 'NONE', #5006, #9071, #12441, .T. ) ;
#13961=EDGE_LOOP ( 'NONE', ( #282, #9864 ) ) ;
#13966=ORIENTED_EDGE ( 'NONE', *, *, #13959, .T. ) ;
#14002=CARTESIAN_POINT ( 'NONE',  ( 0.000000000000000000, 0.000000000000000000, 11.75000000000000000 ) ) ;
#14016=EDGE_CURVE ( 'NONE', #4963, #7321, #3401, .T. ) ;
#14021=CYLINDRICAL_SURFACE ( 'NONE', #12811, 9.999999999999996447 ) ;
#14023=AXIS2_PLACEMENT_3D ( 'NONE', #8015, #10209, #5784 ) ;
#14039=AXIS2_PLACEMENT_3D ( 'NONE', #10508, #9418, #5077 ) ;
#14045=CIRCLE ( 'NONE', #11505, 12.44999999999999929 ) ;
#14056=ADVANCED_FACE ( 'NONE', ( #2840 ), #6664, .T. ) ;
#14097=EDGE_LOOP ( 'NONE', ( #8255, #384, #2979, #5639 ) ) ;
#14103=DIRECTION ( 'NONE',  ( 0.000000000000000000, 0.000000000000000000, -1.000000000000000000 ) ) ;
#14117=DIRECTION ( 'NONE',  ( 1.000000000000000000, 0.000000000000000000, 0.000000000000000000 ) ) ;
#14121=CIRCLE ( 'NONE', #9032, 1.050000000000000488 ) ;
#14126=ORIENTED_EDGE ( 'NONE', *, *, #3644, .F. ) ;
#14139=AXIS2_PLACEMENT_3D ( 'NONE', #3554, #3765, #10358 ) ;
#14161=CARTESIAN_POINT ( 'NONE',  ( -20.63749999999999929, 0.000000000000000000, -9.999999999999996447 ) ) ;
#14164=VERTEX_POINT ( 'NONE', #6087 ) ;
#14166=CIRCLE ( 'NONE', #2799, 10.20000000000000107 ) ;
#14173=ORIENTED_EDGE ( 'NONE', *, *, #6453, .T. ) ;
#14197=CIRCLE ( 'NONE', #1213, 0.2000000000000022593 ) ;
#14203=DIRECTION ( 'NONE',  ( 0.000000000000000000, -1.000000000000000000, 0.000000000000000000 ) ) ;
#14225=EDGE_LOOP ( 'NONE', ( #3287, #10506, #239, #8119 ) ) ;
#14263=DIRECTION ( 'NONE',  ( 1.000000000000000000, 0.000000000000000000, 0.000000000000000000 ) ) ;
#14267=CARTESIAN_POINT ( 'NONE',  ( -2.000000000000001776, 1.564486285910744042E-15, 12.77500000000000213 ) ) ;
#14274=DIRECTION ( 'NONE',  ( 0.000000000000000000, 0.000000000000000000, -1.000000000000000000 ) ) ;
#14281=CIRCLE ( 'NONE', #12446, 10.72500000000000142 ) ;
#14302=AXIS2_PLACEMENT_3D ( 'NONE', #700, #12691, #4063 ) ;
#14404=COLOUR_RGB('Grey',0.48,0.52,0.57);
#14405=FILL_AREA_STYLE_COLOUR('',#14404);
#14406=FILL_AREA_STYLE('',(#14405));
#14407=SURFACE_STYLE_FILL_AREA(#14406);
#14408=SURFACE_SIDE_STYLE('',(#14407));
#14409=SURFACE_STYLE_USAGE(.BOTH.,#14408);
#14410=PRESENTATION_STYLE_ASSIGNMENT((#14409));
ENDSEC;
END-ISO-10303-21;
